ISO-10303-21;
HEADER;
/* Generated by software containing ST-Developer
 * from STEP Tools, Inc. (www.steptools.com) 
 */

FILE_DESCRIPTION(
/* description */ ('PAT-083'),
/* implementation_level */ '2;1');

FILE_NAME(
/* name */ 'Adjuster spring shoe.step',
/* time_stamp */ '2026-10-29T20:18:00-07:00',
/* author */ (''),
/* organization */ (''),
/* preprocessor_version */ 'ST-DEVELOPER v20.2',
/* originating_system */ 'Autodesk Translation Framework v15.17.0.0',
/* authorisation */ '');

FILE_SCHEMA (('AUTOMOTIVE_DESIGN { 1 0 10303 214 3 1 1 }'));
ENDSEC;

DATA;
#10=MECHANICAL_DESIGN_GEOMETRIC_PRESENTATION_REPRESENTATION('',(#242),#8428);
#194=SHAPE_REPRESENTATION_RELATIONSHIP('SRR','None',#8528,#218);
#218=ADVANCED_BREP_SHAPE_REPRESENTATION('',(#266),#8417);
#242=STYLED_ITEM('',(#8705),#266);
#266=MANIFOLD_SOLID_BREP('Body1',#3688);
#340=FACE_BOUND('',#928,.T.);
#423=PLANE('',#4246);
#424=PLANE('',#4250);
#425=PLANE('',#4251);
#625=FACE_OUTER_BOUND('',#923,.T.);
#626=FACE_OUTER_BOUND('',#924,.T.);
#627=FACE_OUTER_BOUND('',#925,.T.);
#628=FACE_OUTER_BOUND('',#926,.T.);
#629=FACE_OUTER_BOUND('',#927,.T.);
#923=EDGE_LOOP('',(#2966,#2967,#2968,#2969));
#924=EDGE_LOOP('',(#2970));
#925=EDGE_LOOP('',(#2971,#2972,#2973,#2974));
#926=EDGE_LOOP('',(#2975));
#927=EDGE_LOOP('',(#2976));
#928=EDGE_LOOP('',(#2977));
#1151=LINE('',#7835,#1395);
#1152=LINE('',#7842,#1396);
#1395=VECTOR('',#5103,0.6);
#1396=VECTOR('',#5112,1.2);
#1664=CIRCLE('',#4244,0.6);
#1665=CIRCLE('',#4245,0.6);
#1666=CIRCLE('',#4248,1.2);
#1667=CIRCLE('',#4249,1.2);
#1877=VERTEX_POINT('',#7832);
#1878=VERTEX_POINT('',#7834);
#1879=VERTEX_POINT('',#7839);
#1880=VERTEX_POINT('',#7841);
#2259=EDGE_CURVE('',#1877,#1877,#1664,.T.);
#2260=EDGE_CURVE('',#1877,#1878,#1151,.T.);
#2261=EDGE_CURVE('',#1878,#1878,#1665,.T.);
#2262=EDGE_CURVE('',#1879,#1879,#1666,.T.);
#2263=EDGE_CURVE('',#1879,#1880,#1152,.T.);
#2264=EDGE_CURVE('',#1880,#1880,#1667,.T.);
#2966=ORIENTED_EDGE('',*,*,#2259,.F.);
#2967=ORIENTED_EDGE('',*,*,#2260,.T.);
#2968=ORIENTED_EDGE('',*,*,#2261,.T.);
#2969=ORIENTED_EDGE('',*,*,#2260,.F.);
#2970=ORIENTED_EDGE('',*,*,#2261,.F.);
#2971=ORIENTED_EDGE('',*,*,#2262,.F.);
#2972=ORIENTED_EDGE('',*,*,#2263,.T.);
#2973=ORIENTED_EDGE('',*,*,#2264,.T.);
#2974=ORIENTED_EDGE('',*,*,#2263,.F.);
#2975=ORIENTED_EDGE('',*,*,#2262,.T.);
#2976=ORIENTED_EDGE('',*,*,#2264,.F.);
#2977=ORIENTED_EDGE('',*,*,#2259,.T.);
#3425=CYLINDRICAL_SURFACE('',#4243,0.6);
#3426=CYLINDRICAL_SURFACE('',#4247,1.2);
#3572=ADVANCED_FACE('',(#625),#3425,.T.);
#3573=ADVANCED_FACE('',(#626),#423,.F.);
#3574=ADVANCED_FACE('',(#627),#3426,.T.);
#3575=ADVANCED_FACE('',(#628),#424,.T.);
#3576=ADVANCED_FACE('',(#629,#340),#425,.F.);
#3688=CLOSED_SHELL('',(#3572,#3573,#3574,#3575,#3576));
#4242=AXIS2_PLACEMENT_3D('',#7830,#5097,#5098);
#4243=AXIS2_PLACEMENT_3D('',#7831,#5099,#5100);
#4244=AXIS2_PLACEMENT_3D('',#7833,#5101,#5102);
#4245=AXIS2_PLACEMENT_3D('',#7836,#5104,#5105);
#4246=AXIS2_PLACEMENT_3D('',#7837,#5106,#5107);
#4247=AXIS2_PLACEMENT_3D('',#7838,#5108,#5109);
#4248=AXIS2_PLACEMENT_3D('',#7840,#5110,#5111);
#4249=AXIS2_PLACEMENT_3D('',#7843,#5113,#5114);
#4250=AXIS2_PLACEMENT_3D('',#7844,#5115,#5116);
#4251=AXIS2_PLACEMENT_3D('',#7845,#5117,#5118);
#5097=DIRECTION('axis',(0.,0.,1.));
#5098=DIRECTION('refdir',(1.,0.,0.));
#5099=DIRECTION('center_axis',(0.,0.,1.));
#5100=DIRECTION('ref_axis',(1.,0.,0.));
#5101=DIRECTION('center_axis',(0.,0.,1.));
#5102=DIRECTION('ref_axis',(1.,0.,0.));
#5103=DIRECTION('',(0.,0.,-1.));
#5104=DIRECTION('center_axis',(0.,0.,1.));
#5105=DIRECTION('ref_axis',(1.,0.,0.));
#5106=DIRECTION('center_axis',(0.,0.,1.));
#5107=DIRECTION('ref_axis',(1.,0.,0.));
#5108=DIRECTION('center_axis',(0.,0.,1.));
#5109=DIRECTION('ref_axis',(1.,0.,0.));
#5110=DIRECTION('center_axis',(0.,0.,1.));
#5111=DIRECTION('ref_axis',(1.,0.,0.));
#5112=DIRECTION('',(0.,0.,-1.));
#5113=DIRECTION('center_axis',(0.,0.,1.));
#5114=DIRECTION('ref_axis',(1.,0.,0.));
#5115=DIRECTION('center_axis',(0.,0.,1.));
#5116=DIRECTION('ref_axis',(1.,0.,0.));
#5117=DIRECTION('center_axis',(0.,0.,1.));
#5118=DIRECTION('ref_axis',(1.,0.,0.));
#7830=CARTESIAN_POINT('',(0.,0.,0.));
#7831=CARTESIAN_POINT('Origin',(0.,0.,7.2));
#7832=CARTESIAN_POINT('',(-0.6,-7.34788079488412E-17,7.6));
#7833=CARTESIAN_POINT('Origin',(0.,0.,7.6));
#7834=CARTESIAN_POINT('',(-0.6,-7.34788079488412E-17,7.2));
#7835=CARTESIAN_POINT('',(-0.6,-7.34788079488412E-17,7.2));
#7836=CARTESIAN_POINT('Origin',(0.,0.,7.2));
#7837=CARTESIAN_POINT('Origin',(0.,0.,7.2));
#7838=CARTESIAN_POINT('Origin',(0.,0.,7.6));
#7839=CARTESIAN_POINT('',(-1.2,-1.46957615897682E-16,8.));
#7840=CARTESIAN_POINT('Origin',(0.,0.,8.));
#7841=CARTESIAN_POINT('',(-1.2,-1.46957615897682E-16,7.6));
#7842=CARTESIAN_POINT('',(-1.2,-1.46957615897682E-16,7.6));
#7843=CARTESIAN_POINT('Origin',(0.,0.,7.6));
#7844=CARTESIAN_POINT('Origin',(0.,0.,8.));
#7845=CARTESIAN_POINT('Origin',(0.,0.,7.6));
#8391=UNCERTAINTY_MEASURE_WITH_UNIT(LENGTH_MEASURE(0.001),#8429,
'DISTANCE_ACCURACY_VALUE',
'Maximum model space distance between geometric entities at asserted c
onnectivities');
#8402=UNCERTAINTY_MEASURE_WITH_UNIT(LENGTH_MEASURE(0.001),#8429,
'DISTANCE_ACCURACY_VALUE',
'Maximum model space distance between geometric entities at asserted c
onnectivities');
#8417=(
GEOMETRIC_REPRESENTATION_CONTEXT(3)
GLOBAL_UNCERTAINTY_ASSIGNED_CONTEXT((#8391))
GLOBAL_UNIT_ASSIGNED_CONTEXT((#8429,#8431,#8432))
REPRESENTATION_CONTEXT('','3D')
);
#8428=(
GEOMETRIC_REPRESENTATION_CONTEXT(3)
GLOBAL_UNCERTAINTY_ASSIGNED_CONTEXT((#8402))
GLOBAL_UNIT_ASSIGNED_CONTEXT((#8429,#8431,#8432))
REPRESENTATION_CONTEXT('','3D')
);
#8429=(
LENGTH_UNIT()
NAMED_UNIT(*)
SI_UNIT(.CENTI.,.METRE.)
);
#8431=(
NAMED_UNIT(*)
PLANE_ANGLE_UNIT()
SI_UNIT($,.RADIAN.)
);
#8432=(
NAMED_UNIT(*)
SI_UNIT($,.STERADIAN.)
SOLID_ANGLE_UNIT()
);
#8447=SHAPE_DEFINITION_REPRESENTATION(#8472,#8528);
#8472=PRODUCT_DEFINITION_SHAPE('',$,#8554);
#8528=SHAPE_REPRESENTATION('',(#4242),#8417);
#8539=PRODUCT_DEFINITION_CONTEXT('part definition',#8616,'design');
#8554=PRODUCT_DEFINITION('Adjuster spring shoe',
'Adjuster spring shoe',#8579,#8539);
#8579=PRODUCT_DEFINITION_FORMATION('',$,#8632);
#8616=APPLICATION_CONTEXT(
'Core Data for Automotive Mechanical Design Process');
#8617=PRODUCT_CONTEXT('part definition',#8616,'mechanical');
#8632=PRODUCT('Adjuster spring shoe','Adjuster spring shoe',
'Adjuster spring shoe',(#8617));
#8699=COLOUR_RGB('Grey',0.48,0.52,0.57);
#8700=FILL_AREA_STYLE_COLOUR('',#8699);
#8701=FILL_AREA_STYLE('',(#8700));
#8702=SURFACE_STYLE_FILL_AREA(#8701);
#8703=SURFACE_SIDE_STYLE('',(#8702));
#8704=SURFACE_STYLE_USAGE(.BOTH.,#8703);
#8705=PRESENTATION_STYLE_ASSIGNMENT((#8704));
ENDSEC;
END-ISO-10303-21;
